ISO-10303-21;
HEADER;
/* Generated by software containing ST-Developer
 * from STEP Tools, Inc. (www.steptools.com) 
 */

FILE_DESCRIPTION(
/* description */ ('Independent two-stage fixed-ring planetary gearbox,24/24/72 teeth,mod
ule2,20deg involutes,three planets per stage,4:1 x4:1=16:1. Native cut
-space/fillet/pattern tooth profiles derived from reusable gear blanks
; shared sun/planet/ring/carrier parts across both stages. Captured br
onze-journal input/carriers, headed retained planet pins, keyed inters
tage drive and modular keyed output interface. Native ideal gear links
; no torque, precision grade, production backlash/fits, lubrication, s
peed or life rating.'),
/* implementation_level */ '2;1');

FILE_NAME(
/* name */ 'Pivot washer.step',
/* time_stamp */ '2026-11-08T19:10:00-08:00',
/* author */ (''),
/* organization */ (''),
/* preprocessor_version */ 'ST-DEVELOPER v20.2',
/* originating_system */ 'Autodesk Translation Framework v15.17.0.0',
/* authorisation */ '');

FILE_SCHEMA (('AUTOMOTIVE_DESIGN { 1 0 10303 214 3 1 1 }'));
ENDSEC;

DATA;
#10=MECHANICAL_DESIGN_GEOMETRIC_PRESENTATION_REPRESENTATION('',(#1176),#259224);
#1136=SHAPE_REPRESENTATION_RELATIONSHIP('SRR','None',#259383,#1156);
#1156=ADVANCED_BREP_SHAPE_REPRESENTATION('',(#1196),#259217);
#1176=STYLED_ITEM('',(#259490),#1196);
#1196=MANIFOLD_SOLID_BREP('Body1',#25163);
#1310=FACE_BOUND('',#4418,.T.);
#1311=FACE_BOUND('',#4420,.T.);
#1672=PLANE('',#27128);
#1673=PLANE('',#27129);
#2962=FACE_OUTER_BOUND('',#4415,.T.);
#2963=FACE_OUTER_BOUND('',#4416,.T.);
#2964=FACE_OUTER_BOUND('',#4417,.T.);
#2965=FACE_OUTER_BOUND('',#4419,.T.);
#4415=EDGE_LOOP('',(#22682,#22683,#22684,#22685));
#4416=EDGE_LOOP('',(#22686,#22687,#22688,#22689));
#4417=EDGE_LOOP('',(#22690));
#4418=EDGE_LOOP('',(#22691));
#4419=EDGE_LOOP('',(#22692));
#4420=EDGE_LOOP('',(#22693));
#5357=CIRCLE('',#27123,5.);
#5358=CIRCLE('',#27124,5.);
#5359=CIRCLE('',#27126,10.);
#5360=CIRCLE('',#27127,10.);
#7770=LINE('',#256005,#8955);
#7771=LINE('',#256011,#8956);
#8955=VECTOR('',#31903,5.);
#8956=VECTOR('',#31910,10.);
#11465=VERTEX_POINT('',#256002);
#11466=VERTEX_POINT('',#256004);
#11467=VERTEX_POINT('',#256008);
#11468=VERTEX_POINT('',#256010);
#15226=EDGE_CURVE('',#11465,#11465,#5357,.T.);
#15227=EDGE_CURVE('',#11465,#11466,#7770,.T.);
#15228=EDGE_CURVE('',#11466,#11466,#5358,.T.);
#15229=EDGE_CURVE('',#11467,#11467,#5359,.T.);
#15230=EDGE_CURVE('',#11467,#11468,#7771,.T.);
#15231=EDGE_CURVE('',#11468,#11468,#5360,.T.);
#22682=ORIENTED_EDGE('',*,*,#15226,.F.);
#22683=ORIENTED_EDGE('',*,*,#15227,.T.);
#22684=ORIENTED_EDGE('',*,*,#15228,.T.);
#22685=ORIENTED_EDGE('',*,*,#15227,.F.);
#22686=ORIENTED_EDGE('',*,*,#15229,.F.);
#22687=ORIENTED_EDGE('',*,*,#15230,.T.);
#22688=ORIENTED_EDGE('',*,*,#15231,.T.);
#22689=ORIENTED_EDGE('',*,*,#15230,.F.);
#22690=ORIENTED_EDGE('',*,*,#15229,.T.);
#22691=ORIENTED_EDGE('',*,*,#15226,.T.);
#22692=ORIENTED_EDGE('',*,*,#15231,.F.);
#22693=ORIENTED_EDGE('',*,*,#15228,.F.);
#23750=CYLINDRICAL_SURFACE('',#27122,5.);
#23751=CYLINDRICAL_SURFACE('',#27125,10.);
#25068=ADVANCED_FACE('',(#2962),#23750,.F.);
#25069=ADVANCED_FACE('',(#2963),#23751,.T.);
#25070=ADVANCED_FACE('',(#2964,#1310),#1672,.T.);
#25071=ADVANCED_FACE('',(#2965,#1311),#1673,.F.);
#25163=CLOSED_SHELL('',(#25068,#25069,#25070,#25071));
#27121=AXIS2_PLACEMENT_3D('',#256000,#31897,#31898);
#27122=AXIS2_PLACEMENT_3D('',#256001,#31899,#31900);
#27123=AXIS2_PLACEMENT_3D('',#256003,#31901,#31902);
#27124=AXIS2_PLACEMENT_3D('',#256006,#31904,#31905);
#27125=AXIS2_PLACEMENT_3D('',#256007,#31906,#31907);
#27126=AXIS2_PLACEMENT_3D('',#256009,#31908,#31909);
#27127=AXIS2_PLACEMENT_3D('',#256012,#31911,#31912);
#27128=AXIS2_PLACEMENT_3D('',#256013,#31913,#31914);
#27129=AXIS2_PLACEMENT_3D('',#256014,#31915,#31916);
#31897=DIRECTION('axis',(0.,0.,1.));
#31898=DIRECTION('refdir',(1.,0.,0.));
#31899=DIRECTION('center_axis',(0.,0.,1.));
#31900=DIRECTION('ref_axis',(1.,0.,0.));
#31901=DIRECTION('center_axis',(0.,0.,-1.));
#31902=DIRECTION('ref_axis',(1.,0.,0.));
#31903=DIRECTION('',(0.,0.,-1.));
#31904=DIRECTION('center_axis',(0.,0.,-1.));
#31905=DIRECTION('ref_axis',(1.,0.,0.));
#31906=DIRECTION('center_axis',(0.,0.,1.));
#31907=DIRECTION('ref_axis',(1.,0.,0.));
#31908=DIRECTION('center_axis',(0.,0.,1.));
#31909=DIRECTION('ref_axis',(1.,0.,0.));
#31910=DIRECTION('',(0.,0.,-1.));
#31911=DIRECTION('center_axis',(0.,0.,1.));
#31912=DIRECTION('ref_axis',(1.,0.,0.));
#31913=DIRECTION('center_axis',(0.,0.,1.));
#31914=DIRECTION('ref_axis',(1.,0.,0.));
#31915=DIRECTION('center_axis',(0.,0.,1.));
#31916=DIRECTION('ref_axis',(1.,0.,0.));
#256000=CARTESIAN_POINT('',(0.,0.,0.));
#256001=CARTESIAN_POINT('Origin',(0.,0.,0.));
#256002=CARTESIAN_POINT('',(-5.,-6.12323399573677E-16,2.));
#256003=CARTESIAN_POINT('Origin',(0.,0.,2.));
#256004=CARTESIAN_POINT('',(-5.,-6.12323399573677E-16,0.));
#256005=CARTESIAN_POINT('',(-5.,-6.12323399573677E-16,0.));
#256006=CARTESIAN_POINT('Origin',(0.,0.,0.));
#256007=CARTESIAN_POINT('Origin',(0.,0.,0.));
#256008=CARTESIAN_POINT('',(-10.,-1.22464679914735E-15,2.));
#256009=CARTESIAN_POINT('Origin',(0.,0.,2.));
#256010=CARTESIAN_POINT('',(-10.,-1.22464679914735E-15,0.));
#256011=CARTESIAN_POINT('',(-10.,-1.22464679914735E-15,0.));
#256012=CARTESIAN_POINT('Origin',(0.,0.,0.));
#256013=CARTESIAN_POINT('Origin',(0.,0.,2.));
#256014=CARTESIAN_POINT('Origin',(0.,0.,0.));
#259195=UNCERTAINTY_MEASURE_WITH_UNIT(LENGTH_MEASURE(0.01),#259225,
'DISTANCE_ACCURACY_VALUE',
'Maximum model space distance between geometric entities at asserted c
onnectivities');
#259202=UNCERTAINTY_MEASURE_WITH_UNIT(LENGTH_MEASURE(0.01),#259225,
'DISTANCE_ACCURACY_VALUE',
'Maximum model space distance between geometric entities at asserted c
onnectivities');
#259217=(
GEOMETRIC_REPRESENTATION_CONTEXT(3)
GLOBAL_UNCERTAINTY_ASSIGNED_CONTEXT((#259195))
GLOBAL_UNIT_ASSIGNED_CONTEXT((#259225,#259227,#259228))
REPRESENTATION_CONTEXT('','3D')
);
#259224=(
GEOMETRIC_REPRESENTATION_CONTEXT(3)
GLOBAL_UNCERTAINTY_ASSIGNED_CONTEXT((#259202))
GLOBAL_UNIT_ASSIGNED_CONTEXT((#259225,#259227,#259228))
REPRESENTATION_CONTEXT('','3D')
);
#259225=(
LENGTH_UNIT()
NAMED_UNIT(*)
SI_UNIT(.MILLI.,.METRE.)
);
#259227=(
NAMED_UNIT(*)
PLANE_ANGLE_UNIT()
SI_UNIT($,.RADIAN.)
);
#259228=(
NAMED_UNIT(*)
SI_UNIT($,.STERADIAN.)
SOLID_ANGLE_UNIT()
);
#259243=SHAPE_DEFINITION_REPRESENTATION(#259264,#259383);
#259264=PRODUCT_DEFINITION_SHAPE('',$,#259405);
#259383=SHAPE_REPRESENTATION('',(#27121),#259217);
#259390=PRODUCT_DEFINITION_CONTEXT('part definition',#259455,'design');
#259405=PRODUCT_DEFINITION('Pivot washer','Pivot washer',#259426,#259390);
#259426=PRODUCT_DEFINITION_FORMATION('',$,#259471);
#259455=APPLICATION_CONTEXT(
'Core Data for Automotive Mechanical Design Process');
#259456=PRODUCT_CONTEXT('part definition',#259455,'mechanical');
#259471=PRODUCT('Pivot washer','Pivot washer',$,(#259456));
#259490=PRESENTATION_STYLE_ASSIGNMENT((#259505));
#259505=SURFACE_STYLE_USAGE(.BOTH.,#259520);
#259520=SURFACE_SIDE_STYLE('',(#259535));
#259535=SURFACE_STYLE_FILL_AREA(#259550);
#259550=FILL_AREA_STYLE('Washer light gray',(#259565));
#259565=FILL_AREA_STYLE_COLOUR('Washer light gray',#259580);
#259580=COLOUR_RGB('Washer light gray',0.725490196078431,0.752941176470588,
0.792156862745098);
ENDSEC;
END-ISO-10303-21;
